ISO-10303-21;
HEADER;
FILE_DESCRIPTION((''),'2;1');
FILE_NAME('GEARBOX_MOUNT_BOLT_M12x65.step','2026-10-01T22:06:14-07:00',(''),(''),'','','');
FILE_SCHEMA (('AUTOMOTIVE_DESIGN { 1 0 10303 214 3 1 1 }'));
ENDSEC;
DATA;
#10=MECHANICAL_DESIGN_GEOMETRIC_PRESENTATION_REPRESENTATION('',(#1030),#50440);
#929=SHAPE_REPRESENTATION_RELATIONSHIP('SRR','None',#50664,#974) ;
#974=ADVANCED_BREP_SHAPE_REPRESENTATION('',(#1083),#50433) ;
#1030=STYLED_ITEM('',(#50883),#1083) ;
#1083=MANIFOLD_SOLID_BREP('GEARBOX_MOUNT_BOLT_M12x65',#28708) ;
#1400=FACE_BOUND('',#5671,.T.) ;
#2297=PLANE('',#32211) ;
#2298=PLANE('',#32212) ;
#2299=PLANE('',#32213) ;
#2300=PLANE('',#32214) ;
#2301=PLANE('',#32215) ;
#2302=PLANE('',#32216) ;
#2303=PLANE('',#32217) ;
#2304=PLANE('',#32218) ;
#2305=PLANE('',#32219) ;
#3819=FACE_OUTER_BOUND('',#5661,.T.) ;
#3820=FACE_OUTER_BOUND('',#5662,.T.) ;
#3821=FACE_OUTER_BOUND('',#5663,.T.) ;
#3822=FACE_OUTER_BOUND('',#5664,.T.) ;
#3823=FACE_OUTER_BOUND('',#5665,.T.) ;
#3824=FACE_OUTER_BOUND('',#5666,.T.) ;
#3825=FACE_OUTER_BOUND('',#5667,.T.) ;
#3826=FACE_OUTER_BOUND('',#5668,.T.) ;
#3827=FACE_OUTER_BOUND('',#5669,.T.) ;
#3828=FACE_OUTER_BOUND('',#5670,.T.) ;
#5661=EDGE_LOOP('',(#26307,#26308,#26309,#26310)) ;
#5662=EDGE_LOOP('',(#26311)) ;
#5663=EDGE_LOOP('',(#26312,#26313,#26314,#26315)) ;
#5664=EDGE_LOOP('',(#26316,#26317,#26318,#26319)) ;
#5665=EDGE_LOOP('',(#26320,#26321,#26322,#26323,#26324,#26325)) ;
#5666=EDGE_LOOP('',(#26326,#26327,#26328,#26329)) ;
#5667=EDGE_LOOP('',(#26330,#26331,#26332,#26333)) ;
#5668=EDGE_LOOP('',(#26334,#26335,#26336,#26337)) ;
#5669=EDGE_LOOP('',(#26338,#26339,#26340,#26341)) ;
#5670=EDGE_LOOP('',(#26342,#26343,#26344,#26345,#26346,#26347)) ;
#5671=EDGE_LOOP('',(#26348)) ;
#8123=LINE('',#49904,#10595) ;
#8124=LINE('',#49910,#10596) ;
#8125=LINE('',#49912,#10597) ;
#8126=LINE('',#49914,#10598) ;
#8127=LINE('',#49915,#10599) ;
#8128=LINE('',#49919,#10600) ;
#8129=LINE('',#49921,#10601) ;
#8130=LINE('',#49923,#10602) ;
#8131=LINE('',#49924,#10603) ;
#8132=LINE('',#49927,#10604) ;
#8133=LINE('',#49928,#10605) ;
#8134=LINE('',#49930,#10606) ;
#8135=LINE('',#49931,#10607) ;
#8136=LINE('',#49934,#10608) ;
#8137=LINE('',#49935,#10609) ;
#8138=LINE('',#49938,#10610) ;
#8139=LINE('',#49939,#10611) ;
#8140=LINE('',#49941,#10612) ;
#8141=LINE('',#49943,#10613) ;
#10595=VECTOR('',#40768,0.6) ;
#10596=VECTOR('',#40775,1.) ;
#10597=VECTOR('',#40776,1.) ;
#10598=VECTOR('',#40777,1.) ;
#10599=VECTOR('',#40778,1.) ;
#10600=VECTOR('',#40781,1.) ;
#10601=VECTOR('',#40782,1.) ;
#10602=VECTOR('',#40783,1.) ;
#10603=VECTOR('',#40784,1.) ;
#10604=VECTOR('',#40787,1.) ;
#10605=VECTOR('',#40788,1.) ;
#10606=VECTOR('',#40789,1.) ;
#10607=VECTOR('',#40790,1.) ;
#10608=VECTOR('',#40793,1.) ;
#10609=VECTOR('',#40794,1.) ;
#10610=VECTOR('',#40797,1.) ;
#10611=VECTOR('',#40798,1.) ;
#10612=VECTOR('',#40801,1.) ;
#10613=VECTOR('',#40804,1.) ;
#11802=CIRCLE('',#32209,0.6) ;
#11803=CIRCLE('',#32210,0.6) ;
#14448=VERTEX_POINT('',#49901) ;
#14449=VERTEX_POINT('',#49903) ;
#14450=VERTEX_POINT('',#49908) ;
#14451=VERTEX_POINT('',#49909) ;
#14452=VERTEX_POINT('',#49911) ;
#14453=VERTEX_POINT('',#49913) ;
#14454=VERTEX_POINT('',#49917) ;
#14455=VERTEX_POINT('',#49918) ;
#14456=VERTEX_POINT('',#49920) ;
#14457=VERTEX_POINT('',#49922) ;
#14458=VERTEX_POINT('',#49926) ;
#14459=VERTEX_POINT('',#49929) ;
#14460=VERTEX_POINT('',#49933) ;
#14461=VERTEX_POINT('',#49937) ;
#18419=EDGE_CURVE('',#14448,#14448,#11802,.T.) ;
#18420=EDGE_CURVE('',#14448,#14449,#8123,.T.) ;
#18421=EDGE_CURVE('',#14449,#14449,#11803,.T.) ;
#18422=EDGE_CURVE('',#14450,#14451,#8124,.T.) ;
#18423=EDGE_CURVE('',#14450,#14452,#8125,.T.) ;
#18424=EDGE_CURVE('',#14453,#14452,#8126,.T.) ;
#18425=EDGE_CURVE('',#14453,#14451,#8127,.T.) ;
#18426=EDGE_CURVE('',#14454,#14455,#8128,.T.) ;
#18427=EDGE_CURVE('',#14454,#14456,#8129,.T.) ;
#18428=EDGE_CURVE('',#14457,#14456,#8130,.T.) ;
#18429=EDGE_CURVE('',#14457,#14455,#8131,.T.) ;
#18430=EDGE_CURVE('',#14458,#14450,#8132,.T.) ;
#18431=EDGE_CURVE('',#14456,#14458,#8133,.T.) ;
#18432=EDGE_CURVE('',#14459,#14454,#8134,.T.) ;
#18433=EDGE_CURVE('',#14452,#14459,#8135,.T.) ;
#18434=EDGE_CURVE('',#14458,#14460,#8136,.T.) ;
#18435=EDGE_CURVE('',#14451,#14460,#8137,.T.) ;
#18436=EDGE_CURVE('',#14459,#14461,#8138,.T.) ;
#18437=EDGE_CURVE('',#14455,#14461,#8139,.T.) ;
#18438=EDGE_CURVE('',#14460,#14457,#8140,.T.) ;
#18439=EDGE_CURVE('',#14461,#14453,#8141,.T.) ;
#26307=ORIENTED_EDGE('',*,*,#18419,.F.) ;
#26308=ORIENTED_EDGE('',*,*,#18420,.T.) ;
#26309=ORIENTED_EDGE('',*,*,#18421,.F.) ;
#26310=ORIENTED_EDGE('',*,*,#18420,.F.) ;
#26311=ORIENTED_EDGE('',*,*,#18419,.T.) ;
#26312=ORIENTED_EDGE('',*,*,#18422,.F.) ;
#26313=ORIENTED_EDGE('',*,*,#18423,.T.) ;
#26314=ORIENTED_EDGE('',*,*,#18424,.F.) ;
#26315=ORIENTED_EDGE('',*,*,#18425,.T.) ;
#26316=ORIENTED_EDGE('',*,*,#18426,.F.) ;
#26317=ORIENTED_EDGE('',*,*,#18427,.T.) ;
#26318=ORIENTED_EDGE('',*,*,#18428,.F.) ;
#26319=ORIENTED_EDGE('',*,*,#18429,.T.) ;
#26320=ORIENTED_EDGE('',*,*,#18423,.F.) ;
#26321=ORIENTED_EDGE('',*,*,#18430,.F.) ;
#26322=ORIENTED_EDGE('',*,*,#18431,.F.) ;
#26323=ORIENTED_EDGE('',*,*,#18427,.F.) ;
#26324=ORIENTED_EDGE('',*,*,#18432,.F.) ;
#26325=ORIENTED_EDGE('',*,*,#18433,.F.) ;
#26326=ORIENTED_EDGE('',*,*,#18434,.F.) ;
#26327=ORIENTED_EDGE('',*,*,#18430,.T.) ;
#26328=ORIENTED_EDGE('',*,*,#18422,.T.) ;
#26329=ORIENTED_EDGE('',*,*,#18435,.T.) ;
#26330=ORIENTED_EDGE('',*,*,#18436,.F.) ;
#26331=ORIENTED_EDGE('',*,*,#18432,.T.) ;
#26332=ORIENTED_EDGE('',*,*,#18426,.T.) ;
#26333=ORIENTED_EDGE('',*,*,#18437,.T.) ;
#26334=ORIENTED_EDGE('',*,*,#18434,.T.) ;
#26335=ORIENTED_EDGE('',*,*,#18438,.T.) ;
#26336=ORIENTED_EDGE('',*,*,#18428,.T.) ;
#26337=ORIENTED_EDGE('',*,*,#18431,.T.) ;
#26338=ORIENTED_EDGE('',*,*,#18424,.T.) ;
#26339=ORIENTED_EDGE('',*,*,#18433,.T.) ;
#26340=ORIENTED_EDGE('',*,*,#18436,.T.) ;
#26341=ORIENTED_EDGE('',*,*,#18439,.T.) ;
#26342=ORIENTED_EDGE('',*,*,#18425,.F.) ;
#26343=ORIENTED_EDGE('',*,*,#18439,.F.) ;
#26344=ORIENTED_EDGE('',*,*,#18437,.F.) ;
#26345=ORIENTED_EDGE('',*,*,#18429,.F.) ;
#26346=ORIENTED_EDGE('',*,*,#18438,.F.) ;
#26347=ORIENTED_EDGE('',*,*,#18435,.F.) ;
#26348=ORIENTED_EDGE('',*,*,#18421,.T.) ;
#27054=CYLINDRICAL_SURFACE('',#32208,0.6) ;
#28554=ADVANCED_FACE('',(#3819),#27054,.T.) ;
#28555=ADVANCED_FACE('',(#3820),#2297,.T.) ;
#28556=ADVANCED_FACE('',(#3821),#2298,.F.) ;
#28557=ADVANCED_FACE('',(#3822),#2299,.F.) ;
#28558=ADVANCED_FACE('',(#3823),#2300,.T.) ;
#28559=ADVANCED_FACE('',(#3824),#2301,.F.) ;
#28560=ADVANCED_FACE('',(#3825),#2302,.F.) ;
#28561=ADVANCED_FACE('',(#3826),#2303,.F.) ;
#28562=ADVANCED_FACE('',(#3827),#2304,.F.) ;
#28563=ADVANCED_FACE('',(#3828,#1400),#2305,.T.) ;
#28708=CLOSED_SHELL('',(#28554,#28555,#28556,#28557,#28558,#28559,#28560,
#28561,#28562,#28563)) ;
#32207=AXIS2_PLACEMENT_3D('',#49899,#40762,#40763) ;
#32208=AXIS2_PLACEMENT_3D('',#49900,#40764,#40765) ;
#32209=AXIS2_PLACEMENT_3D('',#49902,#40766,#40767) ;
#32210=AXIS2_PLACEMENT_3D('',#49905,#40769,#40770) ;
#32211=AXIS2_PLACEMENT_3D('',#49906,#40771,#40772) ;
#32212=AXIS2_PLACEMENT_3D('',#49907,#40773,#40774) ;
#32213=AXIS2_PLACEMENT_3D('',#49916,#40779,#40780) ;
#32214=AXIS2_PLACEMENT_3D('',#49925,#40785,#40786) ;
#32215=AXIS2_PLACEMENT_3D('',#49932,#40791,#40792) ;
#32216=AXIS2_PLACEMENT_3D('',#49936,#40795,#40796) ;
#32217=AXIS2_PLACEMENT_3D('',#49940,#40799,#40800) ;
#32218=AXIS2_PLACEMENT_3D('',#49942,#40802,#40803) ;
#32219=AXIS2_PLACEMENT_3D('',#49944,#40805,#40806) ;
#40762=DIRECTION('axis',(0.,0.,1.)) ;
#40763=DIRECTION('refdir',(1.,0.,0.)) ;
#40764=DIRECTION('center_axis',(0.,0.,-1.)) ;
#40765=DIRECTION('ref_axis',(1.,0.,0.)) ;
#40766=DIRECTION('center_axis',(0.,0.,-1.)) ;
#40767=DIRECTION('ref_axis',(1.,0.,0.)) ;
#40768=DIRECTION('',(0.,0.,1.)) ;
#40769=DIRECTION('center_axis',(0.,0.,1.)) ;
#40770=DIRECTION('ref_axis',(1.,0.,0.)) ;
#40771=DIRECTION('center_axis',(0.,0.,-1.)) ;
#40772=DIRECTION('ref_axis',(1.,0.,0.)) ;
#40773=DIRECTION('center_axis',(-0.5,-0.866025403784439,0.)) ;
#40774=DIRECTION('ref_axis',(-0.866025403784439,0.5,0.)) ;
#40775=DIRECTION('',(0.,0.,-1.)) ;
#40776=DIRECTION('',(0.866025403784439,-0.5,0.)) ;
#40777=DIRECTION('',(0.,0.,1.)) ;
#40778=DIRECTION('',(-0.866025403784439,0.5,0.)) ;
#40779=DIRECTION('center_axis',(0.5,0.866025403784439,0.)) ;
#40780=DIRECTION('ref_axis',(0.866025403784439,-0.5,0.)) ;
#40781=DIRECTION('',(0.,0.,-1.)) ;
#40782=DIRECTION('',(-0.866025403784439,0.5,0.)) ;
#40783=DIRECTION('',(0.,0.,1.)) ;
#40784=DIRECTION('',(0.866025403784439,-0.5,0.)) ;
#40785=DIRECTION('center_axis',(0.,0.,1.)) ;
#40786=DIRECTION('ref_axis',(-1.,0.,0.)) ;
#40787=DIRECTION('',(0.866025403784439,0.5,0.)) ;
#40788=DIRECTION('',(0.,1.,0.)) ;
#40789=DIRECTION('',(-0.866025403784439,-0.5,0.)) ;
#40790=DIRECTION('',(0.,-1.,0.)) ;
#40791=DIRECTION('center_axis',(0.5,-0.866025403784439,0.)) ;
#40792=DIRECTION('ref_axis',(-0.866025403784439,-0.5,0.)) ;
#40793=DIRECTION('',(0.,0.,-1.)) ;
#40794=DIRECTION('',(-0.866025403784439,-0.5,0.)) ;
#40795=DIRECTION('center_axis',(-0.5,0.866025403784439,0.)) ;
#40796=DIRECTION('ref_axis',(0.866025403784439,0.5,0.)) ;
#40797=DIRECTION('',(0.,0.,-1.)) ;
#40798=DIRECTION('',(0.866025403784439,0.5,0.)) ;
#40799=DIRECTION('center_axis',(1.,0.,0.)) ;
#40800=DIRECTION('ref_axis',(0.,-1.,0.)) ;
#40801=DIRECTION('',(0.,-1.,0.)) ;
#40802=DIRECTION('center_axis',(-1.,0.,0.)) ;
#40803=DIRECTION('ref_axis',(0.,1.,0.)) ;
#40804=DIRECTION('',(0.,1.,0.)) ;
#40805=DIRECTION('center_axis',(0.,0.,-1.)) ;
#40806=DIRECTION('ref_axis',(1.,0.,0.)) ;
#49899=CARTESIAN_POINT('',(0.,0.,0.)) ;
#49900=CARTESIAN_POINT('Origin',(0.,0.,-3.1)) ;
#49901=CARTESIAN_POINT('',(-0.6,7.34788079488412E-17,-6.2)) ;
#49902=CARTESIAN_POINT('Origin',(0.,0.,-6.2)) ;
#49903=CARTESIAN_POINT('',(-0.6,7.34788079488412E-17,0.)) ;
#49904=CARTESIAN_POINT('',(-0.6,7.34788079488412E-17,-3.1)) ;
#49905=CARTESIAN_POINT('Origin',(0.,0.,0.)) ;
#49906=CARTESIAN_POINT('Origin',(0.,0.,-6.2)) ;
#49907=CARTESIAN_POINT('Origin',(0.475,0.822724133595217,0.375)) ;
#49908=CARTESIAN_POINT('',(-2.77555756156289E-16,1.09696551146029,0.75)) ;
#49909=CARTESIAN_POINT('',(-2.77555756156289E-16,1.09696551146029,0.)) ;
#49910=CARTESIAN_POINT('',(-2.77555756156289E-16,1.09696551146029,0.375)) ;
#49911=CARTESIAN_POINT('',(0.95,0.548482755730144,0.75)) ;
#49912=CARTESIAN_POINT('',(0.475,0.822724133595217,0.75)) ;
#49913=CARTESIAN_POINT('',(0.95,0.548482755730144,0.)) ;
#49914=CARTESIAN_POINT('',(0.95,0.548482755730144,0.375)) ;
#49915=CARTESIAN_POINT('',(0.475,0.822724133595217,2.77555756156289E-17)) ;
#49916=CARTESIAN_POINT('Origin',(-0.475,-0.822724133595217,0.375)) ;
#49917=CARTESIAN_POINT('',(2.77555756156289E-16,-1.09696551146029,0.75)) ;
#49918=CARTESIAN_POINT('',(2.77555756156289E-16,-1.09696551146029,0.)) ;
#49919=CARTESIAN_POINT('',(2.77555756156289E-16,-1.09696551146029,0.375)) ;
#49920=CARTESIAN_POINT('',(-0.95,-0.548482755730144,0.75)) ;
#49921=CARTESIAN_POINT('',(-0.475,-0.822724133595217,0.75)) ;
#49922=CARTESIAN_POINT('',(-0.95,-0.548482755730144,0.)) ;
#49923=CARTESIAN_POINT('',(-0.95,-0.548482755730144,0.375)) ;
#49924=CARTESIAN_POINT('',(-0.475,-0.822724133595217,2.77555756156289E-17)) ;
#49925=CARTESIAN_POINT('Origin',(0.,0.,0.75)) ;
#49926=CARTESIAN_POINT('',(-0.95,0.548482755730144,0.75)) ;
#49927=CARTESIAN_POINT('',(-0.475,0.822724133595217,0.75)) ;
#49928=CARTESIAN_POINT('',(-0.95,0.,0.75)) ;
#49929=CARTESIAN_POINT('',(0.95,-0.548482755730144,0.75)) ;
#49930=CARTESIAN_POINT('',(0.475,-0.822724133595217,0.75)) ;
#49931=CARTESIAN_POINT('',(0.95,0.,0.75)) ;
#49932=CARTESIAN_POINT('Origin',(-0.475,0.822724133595217,0.375)) ;
#49933=CARTESIAN_POINT('',(-0.95,0.548482755730144,0.)) ;
#49934=CARTESIAN_POINT('',(-0.95,0.548482755730144,0.375)) ;
#49935=CARTESIAN_POINT('',(-0.475,0.822724133595217,-2.77555756156289E-17)) ;
#49936=CARTESIAN_POINT('Origin',(0.475,-0.822724133595217,0.375)) ;
#49937=CARTESIAN_POINT('',(0.95,-0.548482755730144,0.)) ;
#49938=CARTESIAN_POINT('',(0.95,-0.548482755730144,0.375)) ;
#49939=CARTESIAN_POINT('',(0.475,-0.822724133595217,-2.77555756156289E-17)) ;
#49940=CARTESIAN_POINT('Origin',(-0.95,0.,0.375)) ;
#49941=CARTESIAN_POINT('',(-0.95,0.,0.)) ;
#49942=CARTESIAN_POINT('Origin',(0.95,0.,0.375)) ;
#49943=CARTESIAN_POINT('',(0.95,0.,0.)) ;
#49944=CARTESIAN_POINT('Origin',(0.,0.,0.)) ;
#50380=UNCERTAINTY_MEASURE_WITH_UNIT(LENGTH_MEASURE(0.001),#50441,
'DISTANCE_ACCURACY_VALUE',
'Maximum model space distance between geometric entities at asserted c
onnectivities') ;
#50387=UNCERTAINTY_MEASURE_WITH_UNIT(LENGTH_MEASURE(0.001),#50441,
'DISTANCE_ACCURACY_VALUE',
'Maximum model space distance between geometric entities at asserted c
onnectivities') ;
#50433=(
GEOMETRIC_REPRESENTATION_CONTEXT(3)
GLOBAL_UNCERTAINTY_ASSIGNED_CONTEXT((#50380))
GLOBAL_UNIT_ASSIGNED_CONTEXT((#50441,#50443,#50444))
REPRESENTATION_CONTEXT('','3D')
) ;
#50440=(
GEOMETRIC_REPRESENTATION_CONTEXT(3)
GLOBAL_UNCERTAINTY_ASSIGNED_CONTEXT((#50387))
GLOBAL_UNIT_ASSIGNED_CONTEXT((#50441,#50443,#50444))
REPRESENTATION_CONTEXT('','3D')
) ;
#50441=(
LENGTH_UNIT()
NAMED_UNIT(*)
SI_UNIT(.CENTI.,.METRE.)
) ;
#50443=(
NAMED_UNIT(*)
PLANE_ANGLE_UNIT()
SI_UNIT($,.RADIAN.)
) ;
#50444=(
NAMED_UNIT(*)
SI_UNIT($,.STERADIAN.)
SOLID_ANGLE_UNIT()
) ;
#50490=SHAPE_DEFINITION_REPRESENTATION(#50586,#50664) ;
#50586=PRODUCT_DEFINITION_SHAPE('',$,#50717) ;
#50664=SHAPE_REPRESENTATION('',(#32207),#50433) ;
#50671=PRODUCT_DEFINITION_CONTEXT('part definition',#50829,'design') ;
#50717=PRODUCT_DEFINITION('GEARBOX_MOUNT_BOLT_M12x65',
'GEARBOX_MOUNT_BOLT_M12x65',#50769,#50671) ;
#50769=PRODUCT_DEFINITION_FORMATION('',$,#50876) ;
#50829=APPLICATION_CONTEXT(
'Core Data for Automotive Mechanical Design Process') ;
#50830=PRODUCT_CONTEXT('part definition',#50829,'mechanical') ;
#50876=PRODUCT('GEARBOX_MOUNT_BOLT_M12x65','GEARBOX_MOUNT_BOLT_M12x65',$,
(#50830)) ;
#50883=PRESENTATION_STYLE_ASSIGNMENT((#50890)) ;
#50890=SURFACE_STYLE_USAGE(.BOTH.,#50897) ;
#50897=SURFACE_SIDE_STYLE('',(#50904)) ;
#50904=SURFACE_STYLE_FILL_AREA(#50911) ;
#50911=FILL_AREA_STYLE('Steel - Satin',(#50918)) ;
#50918=FILL_AREA_STYLE_COLOUR('Steel - Satin',#50925) ;
#50925=COLOUR_RGB('Steel - Satin', 0.31764706, 0.68627451, 0.89019608) ;
ENDSEC;
END-ISO-10303-21;
